ISO-10303-21;
HEADER;
FILE_DESCRIPTION (('STEP AP214'),
    '1' );
FILE_NAME ('connecting rod.step',
    '2026-10-28T16:30:29',
    ( '' ),
    ( '' ),
    'SwSTEP 2.0',
    'SolidWorks 2025',
    '' );
FILE_SCHEMA (( 'AUTOMOTIVE_DESIGN' ));
ENDSEC;

DATA;
#10=PRODUCT_CONTEXT ( 'NONE', #4822, 'mechanical' ) ;
#39=CARTESIAN_POINT ( 'NONE',  ( 200.0000000000000000, 11.00000000000000711, 8.660254037844383745 ) ) ;
#62=DIRECTION ( 'NONE',  ( 0.000000000000000000, 0.000000000000000000, 1.000000000000000000 ) ) ;
#122=PLANE ( 'NONE',  #5791 ) ;
#146=DIRECTION ( 'NONE',  ( 0.000000000000000000, 0.000000000000000000, 1.000000000000000000 ) ) ;
#150=FACE_OUTER_BOUND ( 'NONE', #7477, .T. ) ;
#154=EDGE_LOOP ( 'NONE', ( #6396, #3446, #5097, #6881, #3077, #1951, #4826, #5186 ) ) ;
#155=DIRECTION ( 'NONE',  ( 1.853902270198407313E-44, 1.000000000000000000, 0.000000000000000000 ) ) ;
#169=VECTOR ( 'NONE', #1200, 1000.000000000000114 ) ;
#182=CYLINDRICAL_SURFACE ( 'NONE', #7539, 14.00000000000000533 ) ;
#259=CARTESIAN_POINT ( 'NONE',  ( 170.0000000000000000, 0.000000000000000000, 0.000000000000000000 ) ) ;
#333=FACE_OUTER_BOUND ( 'NONE', #5193, .T. ) ;
#374=CARTESIAN_POINT ( 'NONE',  ( 170.0000000000000000, 11.00000000000000533, -8.660254037844387298 ) ) ;
#378=ADVANCED_FACE ( 'NONE', ( #5943 ), #675, .F. ) ;
#419=EDGE_CURVE ( 'NONE', #5657, #1381, #4950, .T. ) ;
#441=VERTEX_POINT ( 'NONE', #6745 ) ;
#453=FACE_OUTER_BOUND ( 'NONE', #2431, .T. ) ;
#461=FACE_OUTER_BOUND ( 'NONE', #4848, .T. ) ;
#511=CARTESIAN_POINT ( 'NONE',  ( 200.0000000000000000, 11.00000000000000533, -8.660254037844387298 ) ) ;
#517=CYLINDRICAL_SURFACE ( 'NONE', #4229, 14.00000000000000533 ) ;
#609=EDGE_CURVE ( 'NONE', #5705, #2768, #1665, .T. ) ;
#611=ORIENTED_EDGE ( 'NONE', *, *, #419, .T. ) ;
#636=EDGE_CURVE ( 'NONE', #1438, #2599, #1086, .T. ) ;
#675=CYLINDRICAL_SURFACE ( 'NONE', #2585, 7.000000000000017764 ) ;
#683=DIRECTION ( 'NONE',  ( 0.000000000000000000, 0.000000000000000000, -1.000000000000000000 ) ) ;
#694=FACE_OUTER_BOUND ( 'NONE', #4550, .T. ) ;
#715=( NAMED_UNIT ( * ) PLANE_ANGLE_UNIT ( ) SI_UNIT ( $, .RADIAN. ) );
#726=FACE_BOUND ( 'NONE', #755, .T. ) ;
#736=DIRECTION ( 'NONE',  ( 1.000000000000000000, 1.853902270198408060E-44, 1.681558157189780485E-44 ) ) ;
#737=CLOSED_SHELL ( 'NONE', ( #2152, #6033, #6330, #1229, #6225, #3190, #5365, #1132, #3312, #378 ) ) ;
#738=VECTOR ( 'NONE', #5916, 1000.000000000000000 ) ;
#755=EDGE_LOOP ( 'NONE', ( #2892, #3943 ) ) ;
#837=FACE_OUTER_BOUND ( 'NONE', #3394, .T. ) ;
#906=AXIS2_PLACEMENT_3D ( 'NONE', #5187, #1254, #5338 ) ;
#965=CARTESIAN_POINT ( 'NONE',  ( 188.0000000000000000, -10.95994505756729254, 7.000000000000017764 ) ) ;
#1024=DIRECTION ( 'NONE',  ( 0.000000000000000000, 0.000000000000000000, -1.000000000000000000 ) ) ;
#1085=SHAPE_DEFINITION_REPRESENTATION ( #1742, #6715 ) ;
#1086=LINE ( 'NONE', #3444, #1724 ) ;
#1114=ORIENTED_EDGE ( 'NONE', *, *, #6201, .F. ) ;
#1132=ADVANCED_FACE ( 'NONE', ( #726, #694 ), #122, .F. ) ;
#1158=ORIENTED_EDGE ( 'NONE', *, *, #1325, .F. ) ;
#1166=VECTOR ( 'NONE', #3510, 1000.000000000000000 ) ;
#1174=LINE ( 'NONE', #5259, #4802 ) ;
#1200=DIRECTION ( 'NONE',  ( 1.681558157189779489E-44, -0.02411877311568872903, 0.9997091000803153271 ) ) ;
#1212=ORIENTED_EDGE ( 'NONE', *, *, #4305, .T. ) ;
#1229=ADVANCED_FACE ( 'NONE', ( #837 ), #5505, .T. ) ;
#1246=( LENGTH_UNIT ( ) NAMED_UNIT ( * ) SI_UNIT ( .MILLI., .METRE. ) );
#1254=DIRECTION ( 'NONE',  ( 1.000000000000000000, 1.853902270198408060E-44, -1.681558157189779738E-44 ) ) ;
#1264=ORIENTED_EDGE ( 'NONE', *, *, #7048, .T. ) ;
#1305=AXIS2_PLACEMENT_3D ( 'NONE', #6613, #155, #2493 ) ;
#1314=ORIENTED_EDGE ( 'NONE', *, *, #3233, .F. ) ;
#1325=EDGE_CURVE ( 'NONE', #5705, #6764, #1910, .T. ) ;
#1326=CARTESIAN_POINT ( 'NONE',  ( 170.0000000000000000, -11.00000000000000355, 8.660254037844387298 ) ) ;
#1327=DIRECTION ( 'NONE',  ( -1.000000000000000000, -1.853902270198408060E-44, -1.681558157189780485E-44 ) ) ;
#1331=DIRECTION ( 'NONE',  ( -1.681558157189779738E-44, 0.000000000000000000, -1.000000000000000000 ) ) ;
#1335=LINE ( 'NONE', #7264, #6348 ) ;
#1340=ORIENTED_EDGE ( 'NONE', *, *, #6213, .F. ) ;
#1362=( NAMED_UNIT ( * ) SI_UNIT ( $, .STERADIAN. ) SOLID_ANGLE_UNIT ( ) );
#1381=VERTEX_POINT ( 'NONE', #2412 ) ;
#1406=DIRECTION ( 'NONE',  ( -1.681558157189779738E-44, 0.000000000000000000, -1.000000000000000000 ) ) ;
#1417=DIRECTION ( 'NONE',  ( 1.000000000000000000, 1.853902270198408060E-44, 1.681558157189780485E-44 ) ) ;
#1438=VERTEX_POINT ( 'NONE', #6787 ) ;
#1468=DIRECTION ( 'NONE',  ( 0.000000000000000000, 0.000000000000000000, 1.000000000000000000 ) ) ;
#1560=DIRECTION ( 'NONE',  ( 1.000000000000000000, 1.853902270198408060E-44, 1.681558157189780485E-44 ) ) ;
#1586=VECTOR ( 'NONE', #5181, 1000.000000000000000 ) ;
#1592=CIRCLE ( 'NONE', #7251, 7.000000000000017764 ) ;
#1631=VERTEX_POINT ( 'NONE', #511 ) ;
#1647=AXIS2_PLACEMENT_3D ( 'NONE', #1726, #5157, #4629 ) ;
#1665=LINE ( 'NONE', #4022, #2230 ) ;
#1704=LINE ( 'NONE', #4096, #169 ) ;
#1718=CARTESIAN_POINT ( 'NONE',  ( 200.0000000000000000, 0.000000000000000000, 0.000000000000000000 ) ) ;
#1724=VECTOR ( 'NONE', #6324, 1000.000000000000000 ) ;
#1726=CARTESIAN_POINT ( 'NONE',  ( 170.0000000000000000, 0.000000000000000000, 0.000000000000000000 ) ) ;
#1742=PRODUCT_DEFINITION_SHAPE ( 'NONE', 'NONE',  #3590 ) ;
#1748=( BOUNDED_CURVE ( )  B_SPLINE_CURVE ( 3, ( #4665, #4546, #2724, #6997 ),
 .UNSPECIFIED., .F., .T. ) 
 B_SPLINE_CURVE_WITH_KNOTS ( ( 4, 4 ),
 ( 0.000000000000000000, 3.141592653589793116 ),
 .UNSPECIFIED. ) 
 CURVE ( )  GEOMETRIC_REPRESENTATION_ITEM ( )  RATIONAL_B_SPLINE_CURVE ( ( 1.000000000000000000, 0.3333333333333333703, 0.3333333333333333703, 1.000000000000000000 ) ) 
 REPRESENTATION_ITEM ( '' )  );
#1749=CARTESIAN_POINT ( 'NONE',  ( 0.000000000000000000, 0.000000000000000000, 0.000000000000000000 ) ) ;
#1758=FACE_BOUND ( 'NONE', #5123, .T. ) ;
#1760=ORIENTED_EDGE ( 'NONE', *, *, #6853, .F. ) ;
#1835=CARTESIAN_POINT ( 'NONE',  ( 200.0000000000000000, 1.714505518806294244E-15, -13.99999999999999822 ) ) ;
#1849=VECTOR ( 'NONE', #4522, 1000.000000000000000 ) ;
#1864=DIRECTION ( 'NONE',  ( 1.000000000000000000, 0.000000000000000000, 0.000000000000000000 ) ) ;
#1910=LINE ( 'NONE', #1326, #3038 ) ;
#1914=AXIS2_PLACEMENT_3D ( 'NONE', #1749, #62, #1864 ) ;
#1951=ORIENTED_EDGE ( 'NONE', *, *, #5642, .F. ) ;
#2034=PRODUCT_DEFINITION_FORMATION_WITH_SPECIFIED_SOURCE ( 'ANY', '', #5056, .NOT_KNOWN. ) ;
#2049=CARTESIAN_POINT ( 'NONE',  ( 202.0000000000000568, -10.95994505756729254, 7.000000000000021316 ) ) ;
#2061=CARTESIAN_POINT ( 'NONE',  ( 200.0000000000000000, 0.000000000000000000, 0.000000000000000000 ) ) ;
#2071=LINE ( 'NONE', #3112, #3386 ) ;
#2097=DIRECTION ( 'NONE',  ( 1.000000000000000000, 1.853902270198408060E-44, 1.681558157189780485E-44 ) ) ;
#2139=EDGE_CURVE ( 'NONE', #3264, #441, #1335, .T. ) ;
#2147=DIRECTION ( 'NONE',  ( 1.000000000000000000, 1.853902270198408060E-44, 1.681558157189780485E-44 ) ) ;
#2152=ADVANCED_FACE ( 'NONE', ( #4888 ), #6687, .F. ) ;
#2186=DIRECTION ( 'NONE',  ( -1.853902270198407313E-44, -1.000000000000000000, 0.000000000000000000 ) ) ;
#2230=VECTOR ( 'NONE', #6896, 1000.000000000000000 ) ;
#2276=AXIS2_PLACEMENT_3D ( 'NONE', #3724, #2097, #6210 ) ;
#2284=VERTEX_POINT ( 'NONE', #4500 ) ;
#2297=AXIS2_PLACEMENT_3D ( 'NONE', #5876, #5151, #6459 ) ;
#2298=( NAMED_UNIT ( * ) SI_UNIT ( $, .STERADIAN. ) SOLID_ANGLE_UNIT ( ) );
#2339=DIRECTION ( 'NONE',  ( -1.853902270198407065E-44, -1.000000000000000000, 3.117444485084782485E-88 ) ) ;
#2344=ADVANCED_BREP_SHAPE_REPRESENTATION ( '', ( #6308, #1914 ), #6340 ) ;
#2347=VERTEX_POINT ( 'NONE', #374 ) ;
#2368=FACE_OUTER_BOUND ( 'NONE', #154, .T. ) ;
#2412=CARTESIAN_POINT ( 'NONE',  ( 188.0000000000000000, 11.00000000000000533, -7.000000000000014211 ) ) ;
#2431=EDGE_LOOP ( 'NONE', ( #4654, #4691 ) ) ;
#2448=EDGE_CURVE ( 'NONE', #441, #2599, #3274, .T. ) ;
#2461=DIRECTION ( 'NONE',  ( 2.119463927291285073E-44, 0.9997091000803153271, 0.02411877311568873250 ) ) ;
#2465=CARTESIAN_POINT ( 'NONE',  ( 170.0000000000000000, 11.00000000000000711, 8.660254037844383745 ) ) ;
#2493=DIRECTION ( 'NONE',  ( 0.000000000000000000, 0.000000000000000000, 1.000000000000000000 ) ) ;
#2519=CIRCLE ( 'NONE', #3501, 14.00000000000000533 ) ;
#2552=ORIENTED_EDGE ( 'NONE', *, *, #3301, .T. ) ;
#2580=CARTESIAN_POINT ( 'NONE',  ( 170.0000000000000000, 0.000000000000000000, 0.000000000000000000 ) ) ;
#2585=AXIS2_PLACEMENT_3D ( 'NONE', #5449, #7214, #1468 ) ;
#2599=VERTEX_POINT ( 'NONE', #3033 ) ;
#2676=DIRECTION ( 'NONE',  ( -1.853902270198407313E-44, -1.000000000000000000, 0.000000000000000000 ) ) ;
#2724=CARTESIAN_POINT ( 'NONE',  ( 173.9999999999999716, -10.95994505756729254, 7.000000000000016875 ) ) ;
#2738=ORIENTED_EDGE ( 'NONE', *, *, #5642, .T. ) ;
#2768=VERTEX_POINT ( 'NONE', #4258 ) ;
#2808=PLANE ( 'NONE',  #1647 ) ;
#2830=CARTESIAN_POINT ( 'NONE',  ( 188.0000000000000000, -14.00000000000000711, 7.000000000000017764 ) ) ;
#2833=ORIENTED_EDGE ( 'NONE', *, *, #609, .T. ) ;
#2892=ORIENTED_EDGE ( 'NONE', *, *, #6853, .T. ) ;
#2907=DIRECTION ( 'NONE',  ( 1.000000000000000000, 1.853902270198408060E-44, 1.681558157189780485E-44 ) ) ;
#2922=ORIENTED_EDGE ( 'NONE', *, *, #419, .F. ) ;
#2939=SHAPE_REPRESENTATION_RELATIONSHIP ( 'NONE' , 'NONE' ,  #6715, #2344 ) ;
#2950=DIRECTION ( 'NONE',  ( 1.000000000000000000, 1.853902270198408060E-44, 1.681558157189780485E-44 ) ) ;
#2953=VECTOR ( 'NONE', #4884, 1000.000000000000000 ) ;
#3033=CARTESIAN_POINT ( 'NONE',  ( -2.354181420065692281E-43, -1.853902270198407045E-42, 13.99999999999999822 ) ) ;
#3038=VECTOR ( 'NONE', #5490, 1000.000000000000114 ) ;
#3052=ORIENTED_EDGE ( 'NONE', *, *, #5811, .T. ) ;
#3077=ORIENTED_EDGE ( 'NONE', *, *, #4305, .F. ) ;
#3112=CARTESIAN_POINT ( 'NONE',  ( 170.0000000000000000, 11.00000000000000711, 8.660254037844383745 ) ) ;
#3188=DIRECTION ( 'NONE',  ( -1.681558157189779738E-44, 0.000000000000000000, -1.000000000000000000 ) ) ;
#3190=ADVANCED_FACE ( 'NONE', ( #1758, #150 ), #6610, .F. ) ;
#3194=DIRECTION ( 'NONE',  ( 1.000000000000000000, 1.853902270198408060E-44, 1.681558157189780485E-44 ) ) ;
#3233=EDGE_CURVE ( 'NONE', #2347, #1631, #5953, .T. ) ;
#3238=APPLICATION_CONTEXT ( 'automotive_design' ) ;
#3249=MECHANICAL_DESIGN_GEOMETRIC_PRESENTATION_REPRESENTATION('',(#6566),#5335);
#3262=CARTESIAN_POINT ( 'NONE',  ( 188.0000000000000000, 11.00000000000000533, 0.000000000000000000 ) ) ;
#3264=VERTEX_POINT ( 'NONE', #1835 ) ;
#3274=CIRCLE ( 'NONE', #2297, 14.00000000000000533 ) ;
#3301=EDGE_CURVE ( 'NONE', #3944, #1381, #1592, .T. ) ;
#3312=ADVANCED_FACE ( 'NONE', ( #333 ), #5610, .T. ) ;
#3338=EDGE_CURVE ( 'NONE', #4912, #2347, #4416, .T. ) ;
#3386=VECTOR ( 'NONE', #1417, 1000.000000000000000 ) ;
#3394=EDGE_LOOP ( 'NONE', ( #4025, #4543, #3052, #3982, #1212, #5533 ) ) ;
#3421=LINE ( 'NONE', #2830, #1586 ) ;
#3444=CARTESIAN_POINT ( 'NONE',  ( 200.0000000000000000, 0.000000000000000000, 14.00000000000000533 ) ) ;
#3446=ORIENTED_EDGE ( 'NONE', *, *, #2139, .T. ) ;
#3500=CIRCLE ( 'NONE', #4736, 7.000000000000017764 ) ;
#3501=AXIS2_PLACEMENT_3D ( 'NONE', #3922, #2147, #4973 ) ;
#3510=DIRECTION ( 'NONE',  ( -1.681558157189779738E-44, 0.000000000000000000, -1.000000000000000000 ) ) ;
#3528=DIRECTION ( 'NONE',  ( 0.000000000000000000, 0.000000000000000000, 1.000000000000000000 ) ) ;
#3570=EDGE_CURVE ( 'NONE', #2284, #3944, #3421, .T. ) ;
#3585=EDGE_CURVE ( 'NONE', #6764, #6974, #1174, .T. ) ;
#3590=PRODUCT_DEFINITION ( 'UNKNOWN', '', #2034, #4187 ) ;
#3724=CARTESIAN_POINT ( 'NONE',  ( 200.0000000000000000, 0.000000000000000000, 0.000000000000000000 ) ) ;
#3750=AXIS2_PLACEMENT_3D ( 'NONE', #6839, #1560, #6256 ) ;
#3799=( LENGTH_UNIT ( ) NAMED_UNIT ( * ) SI_UNIT ( .MILLI., .METRE. ) );
#3841=CARTESIAN_POINT ( 'NONE',  ( 170.0000000000000000, 11.00000000000000711, 8.660254037844383745 ) ) ;
#3922=CARTESIAN_POINT ( 'NONE',  ( 0.000000000000000000, 0.000000000000000000, 0.000000000000000000 ) ) ;
#3925=ORIENTED_EDGE ( 'NONE', *, *, #4586, .T. ) ;
#3943=ORIENTED_EDGE ( 'NONE', *, *, #5243, .T. ) ;
#3944=VERTEX_POINT ( 'NONE', #6823 ) ;
#3982=ORIENTED_EDGE ( 'NONE', *, *, #4586, .F. ) ;
#4022=CARTESIAN_POINT ( 'NONE',  ( 170.0000000000000000, -10.56957438397690474, -9.180637088000993984 ) ) ;
#4025=ORIENTED_EDGE ( 'NONE', *, *, #4094, .F. ) ;
#4045=ORIENTED_EDGE ( 'NONE', *, *, #6213, .T. ) ;
#4094=EDGE_CURVE ( 'NONE', #2768, #6974, #1704, .T. ) ;
#4096=CARTESIAN_POINT ( 'NONE',  ( 200.0000000000000000, -11.00000000000000355, 8.660254037844387298 ) ) ;
#4097=ORIENTED_EDGE ( 'NONE', *, *, #6201, .T. ) ;
#4112=CARTESIAN_POINT ( 'NONE',  ( 170.0000000000000000, 11.00000000000000711, 8.660254037844383745 ) ) ;
#4129=ORIENTED_EDGE ( 'NONE', *, *, #3338, .F. ) ;
#4151=EDGE_CURVE ( 'NONE', #2347, #4912, #5201, .T. ) ;
#4187=PRODUCT_DEFINITION_CONTEXT ( 'detailed design', #3238, 'design' ) ;
#4195=ORIENTED_EDGE ( 'NONE', *, *, #3570, .T. ) ;
#4214=ORIENTED_EDGE ( 'NONE', *, *, #3585, .T. ) ;
#4229=AXIS2_PLACEMENT_3D ( 'NONE', #4798, #7557, #3528 ) ;
#4236=CIRCLE ( 'NONE', #3750, 14.00000000000000711 ) ;
#4258=CARTESIAN_POINT ( 'NONE',  ( 200.0000000000000000, -10.56957438397690829, -9.180637088000986878 ) ) ;
#4268=AXIS2_PLACEMENT_3D ( 'NONE', #4892, #7306, #3188 ) ;
#4305=EDGE_CURVE ( 'NONE', #6424, #1438, #5478, .T. ) ;
#4317=CARTESIAN_POINT ( 'NONE',  ( 200.0000000000000000, -11.00000000000000355, 8.660254037844387298 ) ) ;
#4335=FACE_OUTER_BOUND ( 'NONE', #7396, .T. ) ;
#4404=CARTESIAN_POINT ( 'NONE',  ( 202.0000000000000568, -10.62218397927710356, -7.000000000000018652 ) ) ;
#4416=LINE ( 'NONE', #3841, #2953 ) ;
#4500=CARTESIAN_POINT ( 'NONE',  ( 188.0000000000000000, -10.95994505756729254, 7.000000000000017764 ) ) ;
#4516=CARTESIAN_POINT ( 'NONE',  ( 188.0000000000000000, -10.62218397927710356, -7.000000000000017764 ) ) ;
#4522=DIRECTION ( 'NONE',  ( 1.853902270198407313E-44, 1.000000000000000000, 0.000000000000000000 ) ) ;
#4543=ORIENTED_EDGE ( 'NONE', *, *, #6352, .T. ) ;
#4546=CARTESIAN_POINT ( 'NONE',  ( 173.9999999999999716, -10.62218397927710356, -7.000000000000018652 ) ) ;
#4550=EDGE_LOOP ( 'NONE', ( #6044, #7318, #1158, #2833 ) ) ;
#4575=PLANE ( 'NONE',  #906 ) ;
#4586=EDGE_CURVE ( 'NONE', #6424, #1631, #6394, .T. ) ;
#4629=DIRECTION ( 'NONE',  ( -1.681558157189779738E-44, 0.000000000000000000, -1.000000000000000000 ) ) ;
#4654=ORIENTED_EDGE ( 'NONE', *, *, #7048, .F. ) ;
#4665=CARTESIAN_POINT ( 'NONE',  ( 188.0000000000000000, -10.62218397927710356, -7.000000000000017764 ) ) ;
#4691=ORIENTED_EDGE ( 'NONE', *, *, #2448, .F. ) ;
#4728=AXIS2_PLACEMENT_3D ( 'NONE', #1718, #2950, #683 ) ;
#4736=AXIS2_PLACEMENT_3D ( 'NONE', #5115, #2186, #1024 ) ;
#4798=CARTESIAN_POINT ( 'NONE',  ( 200.0000000000000000, 0.000000000000000000, 0.000000000000000000 ) ) ;
#4802=VECTOR ( 'NONE', #2907, 1000.000000000000000 ) ;
#4822=APPLICATION_CONTEXT ( 'automotive_design' ) ;
#4826=ORIENTED_EDGE ( 'NONE', *, *, #4151, .F. ) ;
#4837=ORIENTED_EDGE ( 'NONE', *, *, #5243, .F. ) ;
#4848=EDGE_LOOP ( 'NONE', ( #5819, #5347 ) ) ;
#4855=CARTESIAN_POINT ( 'NONE',  ( 170.0000000000000000, -11.00000000000000355, 8.660254037844387298 ) ) ;
#4884=DIRECTION ( 'NONE',  ( -1.681558157189779738E-44, 0.000000000000000000, -1.000000000000000000 ) ) ;
#4888=FACE_OUTER_BOUND ( 'NONE', #6370, .T. ) ;
#4892=CARTESIAN_POINT ( 'NONE',  ( 200.0000000000000000, 0.000000000000000000, 0.000000000000000000 ) ) ;
#4912=VERTEX_POINT ( 'NONE', #2465 ) ;
#4950=LINE ( 'NONE', #5600, #1849 ) ;
#4973=DIRECTION ( 'NONE',  ( -1.681558157189779489E-44, 0.000000000000000000, -1.000000000000000000 ) ) ;
#5056=PRODUCT ( 'connecting rod', 'connecting rod', '', ( #10 ) ) ;
#5097=ORIENTED_EDGE ( 'NONE', *, *, #2448, .T. ) ;
#5101=CIRCLE ( 'NONE', #2276, 14.00000000000000533 ) ;
#5103=( BOUNDED_CURVE ( )  B_SPLINE_CURVE ( 3, ( #965, #2049, #4404, #4516 ),
 .UNSPECIFIED., .F., .T. ) 
 B_SPLINE_CURVE_WITH_KNOTS ( ( 4, 4 ),
 ( 3.141592653589793116, 6.283185307179586232 ),
 .UNSPECIFIED. ) 
 CURVE ( )  GEOMETRIC_REPRESENTATION_ITEM ( )  RATIONAL_B_SPLINE_CURVE ( ( 1.000000000000000000, 0.3333333333333333703, 0.3333333333333333703, 1.000000000000000000 ) ) 
 REPRESENTATION_ITEM ( '' )  );
#5115=CARTESIAN_POINT ( 'NONE',  ( 188.0000000000000000, 11.00000000000000533, 0.000000000000000000 ) ) ;
#5118=CARTESIAN_POINT ( 'NONE',  ( 170.0000000000000000, -10.56957438397690474, -9.180637088000993984 ) ) ;
#5123=EDGE_LOOP ( 'NONE', ( #2552, #4045 ) ) ;
#5126=EDGE_CURVE ( 'NONE', #1438, #6974, #5947, .T. ) ;
#5151=DIRECTION ( 'NONE',  ( 1.000000000000000000, 1.853902270198408060E-44, 1.681558157189780485E-44 ) ) ;
#5157=DIRECTION ( 'NONE',  ( 1.000000000000000000, 1.853902270198408060E-44, -1.681558157189779738E-44 ) ) ;
#5181=DIRECTION ( 'NONE',  ( 1.853902270198407313E-44, 1.000000000000000000, 0.000000000000000000 ) ) ;
#5186=ORIENTED_EDGE ( 'NONE', *, *, #3233, .T. ) ;
#5187=CARTESIAN_POINT ( 'NONE',  ( 0.000000000000000000, 0.000000000000000000, 0.000000000000000000 ) ) ;
#5193=EDGE_LOOP ( 'NONE', ( #4097, #6319 ) ) ;
#5201=CIRCLE ( 'NONE', #6021, 14.00000000000000533 ) ;
#5229=AXIS2_PLACEMENT_3D ( 'NONE', #6850, #7426, #6188 ) ;
#5243=EDGE_CURVE ( 'NONE', #5657, #2284, #1748, .T. ) ;
#5259=CARTESIAN_POINT ( 'NONE',  ( 170.0000000000000000, -11.00000000000000355, 8.660254037844387298 ) ) ;
#5289=( NAMED_UNIT ( * ) PLANE_ANGLE_UNIT ( ) SI_UNIT ( $, .RADIAN. ) );
#5335=( GEOMETRIC_REPRESENTATION_CONTEXT ( 3 ) GLOBAL_UNCERTAINTY_ASSIGNED_CONTEXT ( ( #7025 ) ) GLOBAL_UNIT_ASSIGNED_CONTEXT ( ( #3799, #715, #1362 ) ) REPRESENTATION_CONTEXT ( 'NONE', 'WORKASPACE' ) );
#5338=DIRECTION ( 'NONE',  ( -1.681558157189779738E-44, 0.000000000000000000, -1.000000000000000000 ) ) ;
#5347=ORIENTED_EDGE ( 'NONE', *, *, #3338, .T. ) ;
#5365=ADVANCED_FACE ( 'NONE', ( #461 ), #2808, .T. ) ;
#5449=CARTESIAN_POINT ( 'NONE',  ( 188.0000000000000000, -14.00000000000000711, 0.000000000000000000 ) ) ;
#5478=CIRCLE ( 'NONE', #5229, 14.00000000000000533 ) ;
#5480=DIRECTION ( 'NONE',  ( 0.000000000000000000, 0.000000000000000000, -1.000000000000000000 ) ) ;
#5490=DIRECTION ( 'NONE',  ( 1.681558157189779489E-44, -0.02411877311568872903, 0.9997091000803153271 ) ) ;
#5501=DIRECTION ( 'NONE',  ( -1.000000000000000000, -1.853902270198408060E-44, -1.681558157189780485E-44 ) ) ;
#5505=PLANE ( 'NONE',  #4268 ) ;
#5533=ORIENTED_EDGE ( 'NONE', *, *, #5126, .T. ) ;
#5556=ORIENTED_EDGE ( 'NONE', *, *, #636, .T. ) ;
#5570=DIRECTION ( 'NONE',  ( 0.000000000000000000, 0.000000000000000000, -1.000000000000000000 ) ) ;
#5577=CIRCLE ( 'NONE', #4728, 14.00000000000000533 ) ;
#5600=CARTESIAN_POINT ( 'NONE',  ( 188.0000000000000000, -14.00000000000000711, -7.000000000000017764 ) ) ;
#5610=PLANE ( 'NONE',  #6639 ) ;
#5642=EDGE_CURVE ( 'NONE', #4912, #6424, #2071, .T. ) ;
#5657=VERTEX_POINT ( 'NONE', #6384 ) ;
#5666=ORIENTED_EDGE ( 'NONE', *, *, #609, .F. ) ;
#5705=VERTEX_POINT ( 'NONE', #5118 ) ;
#5791=AXIS2_PLACEMENT_3D ( 'NONE', #4855, #2461, #7084 ) ;
#5811=EDGE_CURVE ( 'NONE', #3264, #1631, #5577, .T. ) ;
#5819=ORIENTED_EDGE ( 'NONE', *, *, #4151, .T. ) ;
#5857=ORIENTED_EDGE ( 'NONE', *, *, #3301, .F. ) ;
#5876=CARTESIAN_POINT ( 'NONE',  ( 0.000000000000000000, 0.000000000000000000, 0.000000000000000000 ) ) ;
#5916=DIRECTION ( 'NONE',  ( 1.000000000000000000, 1.853902270198408060E-44, 1.681558157189780485E-44 ) ) ;
#5943=FACE_OUTER_BOUND ( 'NONE', #6803, .T. ) ;
#5947=CIRCLE ( 'NONE', #6930, 14.00000000000000533 ) ;
#5953=LINE ( 'NONE', #6499, #738 ) ;
#6021=AXIS2_PLACEMENT_3D ( 'NONE', #2580, #736, #5480 ) ;
#6033=ADVANCED_FACE ( 'NONE', ( #2368 ), #517, .T. ) ;
#6044=ORIENTED_EDGE ( 'NONE', *, *, #4094, .T. ) ;
#6051=AXIS2_PLACEMENT_3D ( 'NONE', #4112, #2339, #1331 ) ;
#6052=ORIENTED_EDGE ( 'NONE', *, *, #2139, .F. ) ;
#6188=DIRECTION ( 'NONE',  ( 0.000000000000000000, 0.000000000000000000, -1.000000000000000000 ) ) ;
#6201=EDGE_CURVE ( 'NONE', #6764, #5705, #4236, .T. ) ;
#6210=DIRECTION ( 'NONE',  ( 0.000000000000000000, 0.000000000000000000, -1.000000000000000000 ) ) ;
#6213=EDGE_CURVE ( 'NONE', #1381, #3944, #3500, .T. ) ;
#6225=ADVANCED_FACE ( 'NONE', ( #453 ), #4575, .F. ) ;
#6256=DIRECTION ( 'NONE',  ( 0.000000000000000000, 0.000000000000000000, -1.000000000000000000 ) ) ;
#6287=CARTESIAN_POINT ( 'NONE',  ( 200.0000000000000000, 11.00000000000000711, 8.660254037844383745 ) ) ;
#6308=MANIFOLD_SOLID_BREP ( 'Cut-Extrude2', #737 ) ;
#6319=ORIENTED_EDGE ( 'NONE', *, *, #1325, .T. ) ;
#6324=DIRECTION ( 'NONE',  ( -1.000000000000000000, -1.853902270198408060E-44, -1.681558157189780485E-44 ) ) ;
#6330=ADVANCED_FACE ( 'NONE', ( #4335 ), #182, .T. ) ;
#6340=( GEOMETRIC_REPRESENTATION_CONTEXT ( 3 ) GLOBAL_UNCERTAINTY_ASSIGNED_CONTEXT ( ( #7104 ) ) GLOBAL_UNIT_ASSIGNED_CONTEXT ( ( #1246, #5289, #2298 ) ) REPRESENTATION_CONTEXT ( 'NONE', 'WORKASPACE' ) );
#6348=VECTOR ( 'NONE', #5501, 1000.000000000000000 ) ;
#6352=EDGE_CURVE ( 'NONE', #2768, #3264, #5101, .T. ) ;
#6370=EDGE_LOOP ( 'NONE', ( #4837, #611, #5857, #7106 ) ) ;
#6384=CARTESIAN_POINT ( 'NONE',  ( 188.0000000000000000, -10.62218397927710356, -7.000000000000017764 ) ) ;
#6394=LINE ( 'NONE', #39, #1166 ) ;
#6396=ORIENTED_EDGE ( 'NONE', *, *, #5811, .F. ) ;
#6424=VERTEX_POINT ( 'NONE', #6287 ) ;
#6459=DIRECTION ( 'NONE',  ( -1.681558157189779489E-44, 0.000000000000000000, -1.000000000000000000 ) ) ;
#6499=CARTESIAN_POINT ( 'NONE',  ( 170.0000000000000000, 11.00000000000000533, -8.660254037844387298 ) ) ;
#6566=STYLED_ITEM('',(#7638),#6308);
#6610=PLANE ( 'NONE',  #6051 ) ;
#6613=CARTESIAN_POINT ( 'NONE',  ( 188.0000000000000000, -14.00000000000000711, 0.000000000000000000 ) ) ;
#6639=AXIS2_PLACEMENT_3D ( 'NONE', #259, #6681, #1406 ) ;
#6681=DIRECTION ( 'NONE',  ( 1.000000000000000000, 1.853902270198408060E-44, -1.681558157189779738E-44 ) ) ;
#6687=CYLINDRICAL_SURFACE ( 'NONE', #1305, 7.000000000000017764 ) ;
#6715=SHAPE_REPRESENTATION ( 'connecting rod', ( #1914 ), #6340 ) ;
#6745=CARTESIAN_POINT ( 'NONE',  ( 2.354181420065691883E-43, 1.714505518806294244E-15, -13.99999999999999822 ) ) ;
#6764=VERTEX_POINT ( 'NONE', #7281 ) ;
#6787=CARTESIAN_POINT ( 'NONE',  ( 200.0000000000000000, -1.853902270198407045E-42, 13.99999999999999822 ) ) ;
#6803=EDGE_LOOP ( 'NONE', ( #2922, #1760, #4195, #1340 ) ) ;
#6823=CARTESIAN_POINT ( 'NONE',  ( 188.0000000000000000, 11.00000000000000533, 7.000000000000014211 ) ) ;
#6839=CARTESIAN_POINT ( 'NONE',  ( 170.0000000000000000, 0.000000000000000000, 0.000000000000000000 ) ) ;
#6850=CARTESIAN_POINT ( 'NONE',  ( 200.0000000000000000, 0.000000000000000000, 0.000000000000000000 ) ) ;
#6853=EDGE_CURVE ( 'NONE', #2284, #5657, #5103, .T. ) ;
#6881=ORIENTED_EDGE ( 'NONE', *, *, #636, .F. ) ;
#6896=DIRECTION ( 'NONE',  ( 1.000000000000000000, 1.853902270198408060E-44, 1.681558157189780485E-44 ) ) ;
#6930=AXIS2_PLACEMENT_3D ( 'NONE', #7232, #3194, #7380 ) ;
#6943=ORIENTED_EDGE ( 'NONE', *, *, #6352, .F. ) ;
#6954=ORIENTED_EDGE ( 'NONE', *, *, #5126, .F. ) ;
#6974=VERTEX_POINT ( 'NONE', #4317 ) ;
#6997=CARTESIAN_POINT ( 'NONE',  ( 188.0000000000000000, -10.95994505756729254, 7.000000000000017764 ) ) ;
#7025=UNCERTAINTY_MEASURE_WITH_UNIT (LENGTH_MEASURE( 1.000000000000000082E-05 ), #3799, 'distance_accuracy_value', 'NONE');
#7048=EDGE_CURVE ( 'NONE', #2599, #441, #2519, .T. ) ;
#7084=DIRECTION ( 'NONE',  ( 1.681558157189779489E-44, -0.02411877311568873250, 0.9997091000803153271 ) ) ;
#7104=UNCERTAINTY_MEASURE_WITH_UNIT (LENGTH_MEASURE( 1.000000000000000082E-05 ), #1246, 'distance_accuracy_value', 'NONE');
#7106=ORIENTED_EDGE ( 'NONE', *, *, #3570, .F. ) ;
#7214=DIRECTION ( 'NONE',  ( 1.853902270198407313E-44, 1.000000000000000000, 0.000000000000000000 ) ) ;
#7232=CARTESIAN_POINT ( 'NONE',  ( 200.0000000000000000, 0.000000000000000000, 0.000000000000000000 ) ) ;
#7251=AXIS2_PLACEMENT_3D ( 'NONE', #3262, #2676, #5570 ) ;
#7264=CARTESIAN_POINT ( 'NONE',  ( 200.0000000000000000, 1.714505518806294835E-15, -14.00000000000000533 ) ) ;
#7281=CARTESIAN_POINT ( 'NONE',  ( 170.0000000000000000, -11.00000000000000355, 8.660254037844387298 ) ) ;
#7306=DIRECTION ( 'NONE',  ( 1.000000000000000000, 1.853902270198408060E-44, -1.681558157189779738E-44 ) ) ;
#7318=ORIENTED_EDGE ( 'NONE', *, *, #3585, .F. ) ;
#7380=DIRECTION ( 'NONE',  ( 0.000000000000000000, 0.000000000000000000, -1.000000000000000000 ) ) ;
#7396=EDGE_LOOP ( 'NONE', ( #6052, #6943, #5666, #1114, #4214, #6954, #5556, #1264 ) ) ;
#7426=DIRECTION ( 'NONE',  ( 1.000000000000000000, 1.853902270198408060E-44, 1.681558157189780485E-44 ) ) ;
#7477=EDGE_LOOP ( 'NONE', ( #3925, #1314, #4129, #2738 ) ) ;
#7539=AXIS2_PLACEMENT_3D ( 'NONE', #2061, #1327, #146 ) ;
#7557=DIRECTION ( 'NONE',  ( -1.000000000000000000, -1.853902270198408060E-44, -1.681558157189780485E-44 ) ) ;
#7632=COLOUR_RGB('Grey',0.48,0.52,0.57);
#7633=FILL_AREA_STYLE_COLOUR('',#7632);
#7634=FILL_AREA_STYLE('',(#7633));
#7635=SURFACE_STYLE_FILL_AREA(#7634);
#7636=SURFACE_SIDE_STYLE('',(#7635));
#7637=SURFACE_STYLE_USAGE(.BOTH.,#7636);
#7638=PRESENTATION_STYLE_ASSIGNMENT((#7637));
ENDSEC;
END-ISO-10303-21;
